ISO-10303-21;
HEADER;
FILE_DESCRIPTION (('STEP AP214'),
    '1' );
FILE_NAME ('socket head cap screw_iso_ISO 4762 M5 x 20 - 20N.step',
    '2026-10-08T13:56:24',
    ( '' ),
    ( '' ),
    'SwSTEP 2.0',
    'SolidWorks 2026',
    '' );
FILE_SCHEMA (( 'AUTOMOTIVE_DESIGN' ));
ENDSEC;

DATA;
#5=FACE_OUTER_BOUND ( 'NONE', #2226, .T. ) ;
#27=FACE_BOUND ( 'NONE', #8966, .T. ) ;
#28=CARTESIAN_POINT ( 'NONE',  ( 2.500000000000000000, -1.768423874527823569, 1.021000000000002794 ) ) ;
#61=CARTESIAN_POINT ( 'NONE',  ( 2.500000000000000000, 2.500728763858895382E-16, -2.041999999999999815 ) ) ;
#91=DIRECTION ( 'NONE',  ( -1.000000000000000000, -0.000000000000000000, -0.000000000000000000 ) ) ;
#92=PLANE ( 'NONE',  #4586 ) ;
#98=DIRECTION ( 'NONE',  ( -1.000000000000000000, -0.000000000000000000, -0.000000000000000000 ) ) ;
#120=EDGE_CURVE ( 'NONE', #12835, #7197, #1963, .T. ) ;
#127=DIRECTION ( 'NONE',  ( -1.000000000000000000, -0.000000000000000000, -0.000000000000000000 ) ) ;
#235=VECTOR ( 'NONE', #12531, 1000.000000000000114 ) ;
#242=CARTESIAN_POINT ( 'NONE',  ( 2.500000000000000000, -1.768423874527823791, -1.020999999999998353 ) ) ;
#266=CARTESIAN_POINT ( 'NONE',  ( 2.500000000000000000, 2.357898499370433054, -1.951563910473907981E-15 ) ) ;
#269=CIRCLE ( 'NONE', #3097, 2.041999999999999815 ) ;
#272=ORIENTED_EDGE ( 'NONE', *, *, #10199, .F. ) ;
#273=CARTESIAN_POINT ( 'NONE',  ( 0.000000000000000000, 0.000000000000000000, 0.000000000000000000 ) ) ;
#327=APPLICATION_CONTEXT ( 'automotive_design' ) ;
#424=EDGE_LOOP ( 'NONE', ( #12881, #12363, #14774, #7098 ) ) ;
#459=CYLINDRICAL_SURFACE ( 'NONE', #12090, 4.250000000000000000 ) ;
#467=DIRECTION ( 'NONE',  ( -1.000000000000000000, -0.000000000000000000, -0.000000000000000000 ) ) ;
#497=VECTOR ( 'NONE', #7170, 1000.000000000000000 ) ;
#506=ORIENTED_EDGE ( 'NONE', *, *, #4910, .T. ) ;
#592=LINE ( 'NONE', #12766, #15405 ) ;
#596=ORIENTED_EDGE ( 'NONE', *, *, #12479, .T. ) ;
#620=DIRECTION ( 'NONE',  ( -1.000000000000000000, -0.000000000000000000, -0.000000000000000000 ) ) ;
#622=ORIENTED_EDGE ( 'NONE', *, *, #6645, .F. ) ;
#636=DIRECTION ( 'NONE',  ( 0.000000000000000000, 0.000000000000000000, 1.000000000000000000 ) ) ;
#641=EDGE_CURVE ( 'NONE', #11474, #10194, #4211, .T. ) ;
#668=DIRECTION ( 'NONE',  ( 0.000000000000000000, -0.5000000000000012212, -0.8660254037844380415 ) ) ;
#672=ORIENTED_EDGE ( 'NONE', *, *, #6802, .T. ) ;
#673=EDGE_CURVE ( 'NONE', #15230, #3781, #13404, .T. ) ;
#676=DIRECTION ( 'NONE',  ( 0.000000000000000000, 1.000000000000000000, -1.471414886128461471E-15 ) ) ;
#712=PRODUCT_DEFINITION_FORMATION_WITH_SPECIFIED_SOURCE ( 'ANY', '', #15460, .NOT_KNOWN. ) ;
#769=DIRECTION ( 'NONE',  ( 0.000000000000000000, 0.000000000000000000, 1.000000000000000000 ) ) ;
#772=PLANE ( 'NONE',  #11770 ) ;
#779=DIRECTION ( 'NONE',  ( 0.000000000000000000, -1.224646799147353454E-16, 1.000000000000000000 ) ) ;
#790=SHAPE_REPRESENTATION ( 'socket head cap screw_iso_ISO 4762 M5 x 20 - 20N', ( #3223 ), #15084 ) ;
#843=DIRECTION ( 'NONE',  ( -1.000000000000000000, -0.000000000000000000, -0.000000000000000000 ) ) ;
#844=DIRECTION ( 'NONE',  ( 0.000000000000000000, 0.000000000000000000, -1.000000000000000000 ) ) ;
#871=SURFACE_STYLE_USAGE ( .BOTH. , #2225 ) ;
#872=ORIENTED_EDGE ( 'NONE', *, *, #6146, .F. ) ;
#874=VECTOR ( 'NONE', #4573, 1000.000000000000000 ) ;
#902=DIRECTION ( 'NONE',  ( 0.000000000000000000, 0.000000000000000000, 1.000000000000000000 ) ) ;
#938=LINE ( 'NONE', #7086, #874 ) ;
#939=AXIS2_PLACEMENT_3D ( 'NONE', #4303, #9243, #3246 ) ;
#967=AXIS2_PLACEMENT_3D ( 'NONE', #14438, #8069, #12965 ) ;
#1002=AXIS2_PLACEMENT_3D ( 'NONE', #8932, #7733, #12625 ) ;
#1031=DIRECTION ( 'NONE',  ( 0.000000000000000000, 0.000000000000000000, -1.000000000000000000 ) ) ;
#1049=CARTESIAN_POINT ( 'NONE',  ( 2.500000000000000000, -1.178949249685213863, 2.042000000000002924 ) ) ;
#1063=DIRECTION ( 'NONE',  ( 0.000000000000000000, -1.287488025362403787E-15, -1.000000000000000000 ) ) ;
#1077=ORIENTED_EDGE ( 'NONE', *, *, #6645, .T. ) ;
#1082=LINE ( 'NONE', #14504, #5613 ) ;
#1095=EDGE_LOOP ( 'NONE', ( #4700, #8534, #7460, #13424, #596 ) ) ;
#1127=FACE_OUTER_BOUND ( 'NONE', #9552, .T. ) ;
#1182=CARTESIAN_POINT ( 'NONE',  ( 2.500000000000000000, 2.357898499370433054, -1.951563910473907981E-15 ) ) ;
#1197=DIRECTION ( 'NONE',  ( -1.000000000000000000, -0.000000000000000000, -0.000000000000000000 ) ) ;
#1198=VECTOR ( 'NONE', #14102, 1000.000000000000000 ) ;
#1202=AXIS2_PLACEMENT_3D ( 'NONE', #273, #7860, #13980 ) ;
#1213=DIRECTION ( 'NONE',  ( 0.000000000000000000, 0.4999999999999993894, -0.8660254037844389297 ) ) ;
#1217=ORIENTED_EDGE ( 'NONE', *, *, #14351, .T. ) ;
#1220=DIRECTION ( 'NONE',  ( -1.000000000000000000, -0.000000000000000000, -0.000000000000000000 ) ) ;
#1244=VECTOR ( 'NONE', #15908, 1000.000000000000000 ) ;
#1265=CARTESIAN_POINT ( 'NONE',  ( 2.500000000000000000, -1.178949249685218303, -2.041999999999998039 ) ) ;
#1296=EDGE_CURVE ( 'NONE', #10322, #15077, #2338, .T. ) ;
#1311=DIRECTION ( 'NONE',  ( 0.000000000000000000, -0.5000000000000011102, -0.8660254037844379305 ) ) ;
#1319=DIRECTION ( 'NONE',  ( 0.000000000000000000, 0.000000000000000000, 1.000000000000000000 ) ) ;
#1323=FACE_OUTER_BOUND ( 'NONE', #7151, .T. ) ;
#1333=AXIS2_PLACEMENT_3D ( 'NONE', #14314, #3242, #9613 ) ;
#1348=ORIENTED_EDGE ( 'NONE', *, *, #4910, .F. ) ;
#1410=CARTESIAN_POINT ( 'NONE',  ( 25.00000000000000000, 0.000000000000000000, 0.000000000000000000 ) ) ;
#1473=ORIENTED_EDGE ( 'NONE', *, *, #6665, .F. ) ;
#1484=PRODUCT_DEFINITION ( 'UNKNOWN', '', #712, #8852 ) ;
#1488=SURFACE_STYLE_USAGE ( .BOTH. , #7730 ) ;
#1504=ORIENTED_EDGE ( 'NONE', *, *, #13260, .T. ) ;
#1523=VERTEX_POINT ( 'NONE', #8254 ) ;
#1527=AXIS2_PLACEMENT_3D ( 'NONE', #7191, #12091, #1031 ) ;
#1620=ORIENTED_EDGE ( 'NONE', *, *, #9961, .F. ) ;
#1665=DIRECTION ( 'NONE',  ( -1.000000000000000000, -0.000000000000000000, -0.000000000000000000 ) ) ;
#1714=ORIENTED_EDGE ( 'NONE', *, *, #120, .T. ) ;
#1749=LINE ( 'NONE', #12726, #1882 ) ;
#1829=ORIENTED_EDGE ( 'NONE', *, *, #7686, .F. ) ;
#1836=DIRECTION ( 'NONE',  ( -1.000000000000000000, -0.000000000000000000, -0.000000000000000000 ) ) ;
#1871=ORIENTED_EDGE ( 'NONE', *, *, #4747, .T. ) ;
#1879=DIRECTION ( 'NONE',  ( 0.000000000000000000, 0.000000000000000000, 1.000000000000000000 ) ) ;
#1882=VECTOR ( 'NONE', #1665, 1000.000000000000000 ) ;
#1888=FACE_BOUND ( 'NONE', #13265, .T. ) ;
#1890=PLANE ( 'NONE',  #14444 ) ;
#1909=CARTESIAN_POINT ( 'NONE',  ( 0.000000000000000000, 1.178949249685213863, -2.042000000000001148 ) ) ;
#1915=DIRECTION ( 'NONE',  ( 0.000000000000000000, 0.000000000000000000, -1.000000000000000000 ) ) ;
#1917=CARTESIAN_POINT ( 'NONE',  ( 5.000000000000002665, 0.000000000000000000, -2.700000000000001066 ) ) ;
#1956=AXIS2_PLACEMENT_3D ( 'NONE', #5648, #14133, #3063 ) ;
#1963=CIRCLE ( 'NONE', #12544, 4.000000000000000000 ) ;
#1969=LINE ( 'NONE', #11661, #8441 ) ;
#1987=CARTESIAN_POINT ( 'NONE',  ( 2.500000000000000000, 0.000000000000000000, 0.000000000000000000 ) ) ;
#2028=VECTOR ( 'NONE', #3808, 1000.000000000000114 ) ;
#2030=ADVANCED_FACE ( 'NONE', ( #12219 ), #3594, .T. ) ;
#2059=DIRECTION ( 'NONE',  ( 0.000000000000000000, 0.000000000000000000, 1.000000000000000000 ) ) ;
#2108=ORIENTED_EDGE ( 'NONE', *, *, #3126, .T. ) ;
#2110=LINE ( 'NONE', #13174, #13653 ) ;
#2137=AXIS2_PLACEMENT_3D ( 'NONE', #8660, #91, #4858 ) ;
#2152=EDGE_CURVE ( 'NONE', #4793, #7552, #14824, .T. ) ;
#2175=CARTESIAN_POINT ( 'NONE',  ( 0.000000000000000000, 0.000000000000000000, 4.000000000000000000 ) ) ;
#2178=STYLED_ITEM ( 'NONE', ( #5790 ), #7752 ) ;
#2205=DIRECTION ( 'NONE',  ( -1.000000000000000000, -0.000000000000000000, -0.000000000000000000 ) ) ;
#2225=SURFACE_SIDE_STYLE ('',( #7097 ) ) ;
#2226=EDGE_LOOP ( 'NONE', ( #14757, #13715, #10358, #5017 ) ) ;
#2229=FACE_OUTER_BOUND ( 'NONE', #11324, .T. ) ;
#2266=CARTESIAN_POINT ( 'NONE',  ( 5.000000000000002665, 3.306546357697854226E-16, 2.700000000000001066 ) ) ;
#2287=DIRECTION ( 'NONE',  ( -1.000000000000000000, -0.000000000000000000, -0.000000000000000000 ) ) ;
#2301=EDGE_CURVE ( 'NONE', #13811, #7787, #12940, .T. ) ;
#2321=LINE ( 'NONE', #14939, #15313 ) ;
#2335=EDGE_CURVE ( 'NONE', #10748, #15162, #13193, .T. ) ;
#2338=LINE ( 'NONE', #1049, #4469 ) ;
#2341=PLANE ( 'NONE',  #14956 ) ;
#2351=CARTESIAN_POINT ( 'NONE',  ( 2.500000000000000000, 0.000000000000000000, 0.000000000000000000 ) ) ;
#2367=CARTESIAN_POINT ( 'NONE',  ( 0.000000000000000000, 1.178949249685218525, 2.041999999999999371 ) ) ;
#2369=LINE ( 'NONE', #5776, #15154 ) ;
#2397=ORIENTED_EDGE ( 'NONE', *, *, #1296, .F. ) ;
#2421=AXIS2_PLACEMENT_3D ( 'NONE', #2946, #7004, #779 ) ;
#2456=CONICAL_SURFACE ( 'NONE', #11001, 2.055000000000000160, 0.7853981633974721488 ) ;
#2488=AXIS2_PLACEMENT_3D ( 'NONE', #13593, #12461, #8933 ) ;
#2493=DIRECTION ( 'NONE',  ( 0.000000000000000000, 0.000000000000000000, -1.000000000000000000 ) ) ;
#2498=CARTESIAN_POINT ( 'NONE',  ( 2.500000000000000000, 0.000000000000000000, 0.000000000000000000 ) ) ;
#2508=CONICAL_SURFACE ( 'NONE', #8226, 2.055000000000000160, 0.7853981633974721488 ) ;
#2545=CARTESIAN_POINT ( 'NONE',  ( 0.2500000000000002220, 0.000000000000000000, 4.250000000000000000 ) ) ;
#2562=DIRECTION ( 'NONE',  ( 0.000000000000000000, 0.000000000000000000, 1.000000000000000000 ) ) ;
#2603=ORIENTED_EDGE ( 'NONE', *, *, #3126, .F. ) ;
#2640=CARTESIAN_POINT ( 'NONE',  ( 5.200000000000002842, 0.000000000000000000, 2.500000000000000888 ) ) ;
#2669=CIRCLE ( 'NONE', #11704, 2.700000000000001066 ) ;
#2679=CARTESIAN_POINT ( 'NONE',  ( 5.200000000000002842, 3.061616997868384127E-16, -2.500000000000000888 ) ) ;
#2744=AXIS2_PLACEMENT_3D ( 'NONE', #6916, #10558, #12951 ) ;
#2765=FACE_OUTER_BOUND ( 'NONE', #8041, .T. ) ;
#2813=EDGE_CURVE ( 'NONE', #10194, #15230, #2321, .T. ) ;
#2893=DIRECTION ( 'NONE',  ( 0.000000000000000000, 1.224646799147353207E-16, 1.000000000000000000 ) ) ;
#2894=DIRECTION ( 'NONE',  ( -1.000000000000000000, -0.000000000000000000, -0.000000000000000000 ) ) ;
#2946=CARTESIAN_POINT ( 'NONE',  ( 0.2500000000000002220, 4.898587196589412829E-16, -4.000000000000000000 ) ) ;
#2987=ORIENTED_EDGE ( 'NONE', *, *, #641, .F. ) ;
#2998=EDGE_CURVE ( 'NONE', #15426, #15162, #1749, .T. ) ;
#3025=CARTESIAN_POINT ( 'NONE',  ( 2.500000000000000000, -1.178949249685213863, 2.042000000000002924 ) ) ;
#3045=CARTESIAN_POINT ( 'NONE',  ( 0.000000000000000000, -1.178949249685213863, 2.042000000000002924 ) ) ;
#3063=DIRECTION ( 'NONE',  ( 0.000000000000000000, 0.000000000000000000, 1.000000000000000000 ) ) ;
#3097=AXIS2_PLACEMENT_3D ( 'NONE', #4641, #2205, #8299 ) ;
#3126=EDGE_CURVE ( 'NONE', #8883, #7552, #11755, .T. ) ;
#3132=DIRECTION ( 'NONE',  ( -1.000000000000000000, -0.000000000000000000, -0.000000000000000000 ) ) ;
#3146=EDGE_CURVE ( 'NONE', #3781, #7386, #938, .T. ) ;
#3168=DIRECTION ( 'NONE',  ( -1.000000000000000000, -0.000000000000000000, -0.000000000000000000 ) ) ;
#3185=DIRECTION ( 'NONE',  ( -1.000000000000000000, -0.000000000000000000, -0.000000000000000000 ) ) ;
#3223=AXIS2_PLACEMENT_3D ( 'NONE', #11897, #11972, #4638 ) ;
#3242=DIRECTION ( 'NONE',  ( 1.000000000000000000, 0.000000000000000000, 0.000000000000000000 ) ) ;
#3243=CARTESIAN_POINT ( 'NONE',  ( 2.500000000000000000, 2.357898499370433054, -1.951563910473907981E-15 ) ) ;
#3244=DIRECTION ( 'NONE',  ( -1.000000000000000000, -0.000000000000000000, -0.000000000000000000 ) ) ;
#3246=DIRECTION ( 'NONE',  ( 0.000000000000000000, 0.000000000000000000, 1.000000000000000000 ) ) ;
#3271=AXIS2_PLACEMENT_3D ( 'NONE', #13828, #3168, #4215 ) ;
#3272=ORIENTED_EDGE ( 'NONE', *, *, #8123, .T. ) ;
#3294=( NAMED_UNIT ( * ) PLANE_ANGLE_UNIT ( ) SI_UNIT ( $, .RADIAN. ) );
#3306=CIRCLE ( 'NONE', #7443, 2.500000000000001332 ) ;
#3313=EDGE_CURVE ( 'NONE', #7552, #12557, #9577, .T. ) ;
#3316=ORIENTED_EDGE ( 'NONE', *, *, #2335, .F. ) ;
#3326=CIRCLE ( 'NONE', #7213, 2.500000000000001332 ) ;
#3335=AXIS2_PLACEMENT_3D ( 'NONE', #5488, #14219, #2893 ) ;
#3358=DIRECTION ( 'NONE',  ( -1.000000000000000000, -0.000000000000000000, -0.000000000000000000 ) ) ;
#3364=ADVANCED_FACE ( 'NONE', ( #1323 ), #9892, .T. ) ;
#3414=ORIENTED_EDGE ( 'NONE', *, *, #15028, .T. ) ;
#3460=CYLINDRICAL_SURFACE ( 'NONE', #9949, 2.500000000000000888 ) ;
#3492=EDGE_CURVE ( 'NONE', #10008, #5750, #2669, .T. ) ;
#3544=PLANE ( 'NONE',  #4876 ) ;
#3555=CARTESIAN_POINT ( 'NONE',  ( 25.00000000000000000, 2.516649172247811061E-16, -2.055000000000000160 ) ) ;
#3564=ORIENTED_EDGE ( 'NONE', *, *, #6146, .T. ) ;
#3591=AXIS2_PLACEMENT_3D ( 'NONE', #15304, #6421, #10055 ) ;
#3594=CYLINDRICAL_SURFACE ( 'NONE', #5991, 2.500000000000000888 ) ;
#3604=ORIENTED_EDGE ( 'NONE', *, *, #2335, .T. ) ;
#3630=DIRECTION ( 'NONE',  ( -0.000000000000000000, 1.471414886128461471E-15, 1.000000000000000000 ) ) ;
#3632=CARTESIAN_POINT ( 'NONE',  ( 2.500000000000000000, 2.357898499370433054, -1.951563910473907981E-15 ) ) ;
#3637=FACE_OUTER_BOUND ( 'NONE', #5751, .T. ) ;
#3658=ORIENTED_EDGE ( 'NONE', *, *, #7294, .T. ) ;
#3715=PLANE ( 'NONE',  #15899 ) ;
#3731=CIRCLE ( 'NONE', #8410, 2.041999999999999815 ) ;
#3781=VERTEX_POINT ( 'NONE', #7380 ) ;
#3797=DIRECTION ( 'NONE',  ( 0.000000000000000000, 0.8660254037844380415, -0.5000000000000011102 ) ) ;
#3808=DIRECTION ( 'NONE',  ( 0.000000000000000000, -0.4999999999999993894, 0.8660254037844389297 ) ) ;
#3825=VECTOR ( 'NONE', #7444, 1000.000000000000114 ) ;
#3829=CIRCLE ( 'NONE', #5397, 4.250000000000000000 ) ;
#3837=CARTESIAN_POINT ( 'NONE',  ( 5.000000000000000888, 0.000000000000000000, 0.000000000000000000 ) ) ;
#3845=AXIS2_PLACEMENT_3D ( 'NONE', #12116, #10995, #15934 ) ;
#3903=PRESENTATION_STYLE_ASSIGNMENT (( #1488 ) ) ;
#3956=ORIENTED_EDGE ( 'NONE', *, *, #10924, .F. ) ;
#3962=EDGE_CURVE ( 'NONE', #10453, #8590, #14879, .T. ) ;
#3975=EDGE_CURVE ( 'NONE', #12212, #9210, #15144, .T. ) ;
#3979=( NAMED_UNIT ( * ) SI_UNIT ( $, .STERADIAN. ) SOLID_ANGLE_UNIT ( ) );
#4009=EDGE_CURVE ( 'NONE', #8590, #9210, #592, .T. ) ;
#4047=DIRECTION ( 'NONE',  ( -1.000000000000000000, -0.000000000000000000, -0.000000000000000000 ) ) ;
#4068=CARTESIAN_POINT ( 'NONE',  ( 2.500000000000000000, 2.357898499370433054, -1.951563910473907981E-15 ) ) ;
#4079=ORIENTED_EDGE ( 'NONE', *, *, #12282, .T. ) ;
#4123=ORIENTED_EDGE ( 'NONE', *, *, #2152, .T. ) ;
#4139=PLANE ( 'NONE',  #3591 ) ;
#4144=EDGE_CURVE ( 'NONE', #7386, #12557, #1969, .T. ) ;
#4164=EDGE_CURVE ( 'NONE', #10322, #8883, #15401, .T. ) ;
#4180=CARTESIAN_POINT ( 'NONE',  ( 24.55500000000002103, 0.000000000000000000, 2.500000000000001332 ) ) ;
#4200=EDGE_LOOP ( 'NONE', ( #13482, #6376, #13438, #14194, #1217 ) ) ;
#4211=CIRCLE ( 'NONE', #2137, 2.041999999999999815 ) ;
#4215=DIRECTION ( 'NONE',  ( 0.000000000000000000, 0.000000000000000000, 1.000000000000000000 ) ) ;
#4218=EDGE_CURVE ( 'NONE', #15077, #11474, #9709, .T. ) ;
#4230=ADVANCED_FACE ( 'NONE', ( #1888, #6829 ), #772, .T. ) ;
#4260=FACE_OUTER_BOUND ( 'NONE', #10880, .T. ) ;
#4268=( GEOMETRIC_REPRESENTATION_CONTEXT ( 3 ) GLOBAL_UNCERTAINTY_ASSIGNED_CONTEXT ( ( #11761 ) ) GLOBAL_UNIT_ASSIGNED_CONTEXT ( ( #13754, #11343, #3979 ) ) REPRESENTATION_CONTEXT ( 'NONE', 'WORKASPACE' ) );
#4276=CIRCLE ( 'NONE', #5302, 0.2000000000000000944 ) ;
#4303=CARTESIAN_POINT ( 'NONE',  ( 0.2500000000000002220, 0.000000000000000000, 0.000000000000000000 ) ) ;
#4306=ORIENTED_EDGE ( 'NONE', *, *, #14944, .T. ) ;
#4388=VECTOR ( 'NONE', #1311, 1000.000000000000114 ) ;
#4408=DIRECTION ( 'NONE',  ( 0.000000000000000000, 0.8660254037844380415, -0.5000000000000012212 ) ) ;
#4456=DIRECTION ( 'NONE',  ( 0.000000000000000000, 0.000000000000000000, 1.000000000000000000 ) ) ;
#4469=VECTOR ( 'NONE', #7281, 1000.000000000000000 ) ;
#4475=FACE_OUTER_BOUND ( 'NONE', #13518, .T. ) ;
#4481=ORIENTED_EDGE ( 'NONE', *, *, #11590, .F. ) ;
#4495=DIRECTION ( 'NONE',  ( 0.000000000000000000, 0.000000000000000000, 1.000000000000000000 ) ) ;
#4520=ORIENTED_EDGE ( 'NONE', *, *, #7044, .F. ) ;
#4531=VECTOR ( 'NONE', #13656, 1000.000000000000114 ) ;
#4573=DIRECTION ( 'NONE',  ( 0.000000000000000000, -1.000000000000000000, 1.287488025362403787E-15 ) ) ;
#4586=AXIS2_PLACEMENT_3D ( 'NONE', #6316, #11232, #1213 ) ;
#4589=PLANE ( 'NONE',  #1527 ) ;
#4605=ORIENTED_EDGE ( 'NONE', *, *, #15904, .F. ) ;
#4623=EDGE_CURVE ( 'NONE', #8700, #13974, #9423, .T. ) ;
#4638=DIRECTION ( 'NONE',  ( 1.000000000000000000, 0.000000000000000000, 0.000000000000000000 ) ) ;
#4641=CARTESIAN_POINT ( 'NONE',  ( 2.500000000000000000, 0.000000000000000000, 0.000000000000000000 ) ) ;
#4681=DIRECTION ( 'NONE',  ( 0.000000000000000000, 0.000000000000000000, 1.000000000000000000 ) ) ;
#4700=ORIENTED_EDGE ( 'NONE', *, *, #12142, .F. ) ;
#4701=CARTESIAN_POINT ( 'NONE',  ( 2.500000000000000000, 1.178949249685213863, -2.042000000000001148 ) ) ;
#4703=CARTESIAN_POINT ( 'NONE',  ( 0.000000000000000000, 2.357898499370433054, -1.951563910473907981E-15 ) ) ;
#4717=ORIENTED_EDGE ( 'NONE', *, *, #4623, .T. ) ;
#4738=PRODUCT_DEFINITION_SHAPE ( 'NONE', 'NONE',  #1484 ) ;
#4747=EDGE_CURVE ( 'NONE', #15077, #8700, #2369, .T. ) ;
#4776=DIRECTION ( 'NONE',  ( 0.000000000000000000, 0.000000000000000000, 1.000000000000000000 ) ) ;
#4793=VERTEX_POINT ( 'NONE', #15885 ) ;
#4845=CARTESIAN_POINT ( 'NONE',  ( -31.74999999999995737, 0.000000000000000000, 0.000000000000000000 ) ) ;
#4858=DIRECTION ( 'NONE',  ( 0.000000000000000000, 0.000000000000000000, 1.000000000000000000 ) ) ;
#4865=LINE ( 'NONE', #14798, #4531 ) ;
#4870=AXIS2_PLACEMENT_3D ( 'NONE', #11110, #14829, #15741 ) ;
#4876=AXIS2_PLACEMENT_3D ( 'NONE', #14709, #3630, #11075 ) ;
#4910=EDGE_CURVE ( 'NONE', #4992, #11474, #1082, .T. ) ;
#4918=ORIENTED_EDGE ( 'NONE', *, *, #7113, .T. ) ;
#4936=FACE_OUTER_BOUND ( 'NONE', #11450, .T. ) ;
#4944=EDGE_CURVE ( 'NONE', #15162, #10748, #8209, .T. ) ;
#4958=CARTESIAN_POINT ( 'NONE',  ( 24.55500000000002103, 0.000000000000000000, 0.000000000000000000 ) ) ;
#4972=ORIENTED_EDGE ( 'NONE', *, *, #13283, .T. ) ;
#4978=PLANE ( 'NONE',  #13512 ) ;
#4992=VERTEX_POINT ( 'NONE', #4068 ) ;
#5017=ORIENTED_EDGE ( 'NONE', *, *, #4944, .T. ) ;
#5018=CARTESIAN_POINT ( 'NONE',  ( 0.000000000000000000, -1.178949249685218303, -2.041999999999998039 ) ) ;
#5031=AXIS2_PLACEMENT_3D ( 'NONE', #6754, #9334, #769 ) ;
#5060=LINE ( 'NONE', #9996, #6116 ) ;
#5075=ORIENTED_EDGE ( 'NONE', *, *, #5320, .T. ) ;
#5184=ORIENTED_EDGE ( 'NONE', *, *, #10490, .F. ) ;
#5205=FACE_OUTER_BOUND ( 'NONE', #6559, .T. ) ;
#5267=PRODUCT_CONTEXT ( 'NONE', #8162, 'mechanical' ) ;
#5280=CIRCLE ( 'NONE', #2421, 0.2500000000000002220 ) ;
#5285=AXIS2_PLACEMENT_3D ( 'NONE', #7288, #3185, #4776 ) ;
#5302=AXIS2_PLACEMENT_3D ( 'NONE', #13899, #10357, #10279 ) ;
#5320=EDGE_CURVE ( 'NONE', #9210, #12212, #6137, .T. ) ;
#5321=VECTOR ( 'NONE', #14541, 999.9999999999998863 ) ;
#5328=VECTOR ( 'NONE', #14495, 1000.000000000000000 ) ;
#5373=DIRECTION ( 'NONE',  ( 0.000000000000000000, 0.000000000000000000, -1.000000000000000000 ) ) ;
#5397=AXIS2_PLACEMENT_3D ( 'NONE', #11674, #5550, #9116 ) ;
#5475=DIRECTION ( 'NONE',  ( 0.000000000000000000, 0.000000000000000000, 1.000000000000000000 ) ) ;
#5486=ORIENTED_EDGE ( 'NONE', *, *, #4747, .F. ) ;
#5488=CARTESIAN_POINT ( 'NONE',  ( 5.200000000000002842, 3.306546357697854719E-16, 2.700000000000001066 ) ) ;
#5501=CARTESIAN_POINT ( 'NONE',  ( 2.500000000000000000, 1.768423874527822681, -1.021000000000002794 ) ) ;
#5533=DIRECTION ( 'NONE',  ( -1.000000000000000000, -0.000000000000000000, -0.000000000000000000 ) ) ;
#5537=EDGE_LOOP ( 'NONE', ( #15900, #14927, #5486, #2397, #5788 ) ) ;
#5550=DIRECTION ( 'NONE',  ( -1.000000000000000000, -0.000000000000000000, -0.000000000000000000 ) ) ;
#5553=CARTESIAN_POINT ( 'NONE',  ( 25.00000000000000000, 0.000000000000000000, 0.000000000000000000 ) ) ;
#5613=VECTOR ( 'NONE', #6021, 1000.000000000000114 ) ;
#5620=DIRECTION ( 'NONE',  ( 0.000000000000000000, 0.5000000000000012212, 0.8660254037844380415 ) ) ;
#5647=CIRCLE ( 'NONE', #9522, 2.041999999999999815 ) ;
#5648=CARTESIAN_POINT ( 'NONE',  ( 25.00000000000000000, 0.000000000000000000, 0.000000000000000000 ) ) ;
#5709=FACE_OUTER_BOUND ( 'NONE', #7700, .T. ) ;
#5748=DIRECTION ( 'NONE',  ( -0.7071067811865306973, 8.659560562355138702E-17, -0.7071067811865643371 ) ) ;
#5750=VERTEX_POINT ( 'NONE', #2266 ) ;
#5751=EDGE_LOOP ( 'NONE', ( #2603, #11786, #8242, #11610, #4123 ) ) ;
#5753=EDGE_CURVE ( 'NONE', #13811, #15784, #15854, .T. ) ;
#5776=CARTESIAN_POINT ( 'NONE',  ( 2.500000000000000000, -1.178949249685213863, 2.042000000000002924 ) ) ;
#5781=ADVANCED_FACE ( 'NONE', ( #7365 ), #92, .T. ) ;
#5788=ORIENTED_EDGE ( 'NONE', *, *, #4164, .T. ) ;
#5790=PRESENTATION_STYLE_ASSIGNMENT (( #871 ) ) ;
#5874=ORIENTED_EDGE ( 'NONE', *, *, #3146, .T. ) ;
#5912=TOROIDAL_SURFACE ( 'NONE', #1002, 2.700000000000001066, 0.2000000000000000111 ) ;
#5934=FACE_OUTER_BOUND ( 'NONE', #1095, .T. ) ;
#5991=AXIS2_PLACEMENT_3D ( 'NONE', #8380, #3358, #15808 ) ;
#5992=ORIENTED_EDGE ( 'NONE', *, *, #4009, .F. ) ;
#6021=DIRECTION ( 'NONE',  ( 0.000000000000000000, -0.4999999999999993894, 0.8660254037844389297 ) ) ;
#6029=ADVANCED_FACE ( 'NONE', ( #13854 ), #9263, .F. ) ;
#6034=FILL_AREA_STYLE_COLOUR ( '', #10947 ) ;
#6075=VECTOR ( 'NONE', #11865, 1000.000000000000000 ) ;
#6116=VECTOR ( 'NONE', #6449, 1000.000000000000000 ) ;
#6137=CIRCLE ( 'NONE', #967, 4.250000000000000000 ) ;
#6146=EDGE_CURVE ( 'NONE', #10453, #12212, #11895, .T. ) ;
#6177=LINE ( 'NONE', #7152, #10031 ) ;
#6241=EDGE_CURVE ( 'NONE', #15294, #12557, #6177, .T. ) ;
#6265=UNCERTAINTY_MEASURE_WITH_UNIT (LENGTH_MEASURE( 1.000000000000000082E-05 ), #7179, 'distance_accuracy_value', 'NONE');
#6316=CARTESIAN_POINT ( 'NONE',  ( 2.500000000000000000, 2.357898499370433054, -1.951563910473907981E-15 ) ) ;
#6325=ADVANCED_FACE ( 'NONE', ( #5934 ), #9252, .F. ) ;
#6376=ORIENTED_EDGE ( 'NONE', *, *, #12142, .T. ) ;
#6400=AXIS2_PLACEMENT_3D ( 'NONE', #6828, #11736, #6756 ) ;
#6421=DIRECTION ( 'NONE',  ( -0.000000000000000000, 0.8660254037844390407, 0.4999999999999993339 ) ) ;
#6436=CARTESIAN_POINT ( 'NONE',  ( 0.2500000000000002220, 5.204748896376250699E-16, -4.250000000000000000 ) ) ;
#6449=DIRECTION ( 'NONE',  ( 0.000000000000000000, 0.4999999999999993339, -0.8660254037844390407 ) ) ;
#6490=EDGE_CURVE ( 'NONE', #10322, #7200, #10052, .T. ) ;
#6559=EDGE_LOOP ( 'NONE', ( #1620, #3316, #4306, #11275 ) ) ;
#6569=ORIENTED_EDGE ( 'NONE', *, *, #6665, .T. ) ;
#6583=AXIS2_PLACEMENT_3D ( 'NONE', #4701, #1063, #13333 ) ;
#6587=ORIENTED_EDGE ( 'NONE', *, *, #1296, .T. ) ;
#6644=CARTESIAN_POINT ( 'NONE',  ( 5.200000000000002842, 0.000000000000000000, 0.000000000000000000 ) ) ;
#6645=EDGE_CURVE ( 'NONE', #11474, #8700, #8504, .T. ) ;
#6665=EDGE_CURVE ( 'NONE', #15230, #15294, #13466, .T. ) ;
#6699=CARTESIAN_POINT ( 'NONE',  ( 24.55500000000002103, 0.000000000000000000, 0.000000000000000000 ) ) ;
#6754=CARTESIAN_POINT ( 'NONE',  ( -31.74999999999995737, 0.000000000000000000, 0.000000000000000000 ) ) ;
#6756=DIRECTION ( 'NONE',  ( 0.000000000000000000, 0.000000000000000000, -1.000000000000000000 ) ) ;
#6802=EDGE_CURVE ( 'NONE', #15426, #15784, #3326, .T. ) ;
#6828=CARTESIAN_POINT ( 'NONE',  ( 2.500000000000000000, 2.357898499370433054, -1.951563910473907981E-15 ) ) ;
#6829=FACE_OUTER_BOUND ( 'NONE', #9619, .T. ) ;
#6834=AXIS2_PLACEMENT_3D ( 'NONE', #11926, #1836, #1915 ) ;
#6876=CIRCLE ( 'NONE', #1956, 2.055000000000000160 ) ;
#6916=CARTESIAN_POINT ( 'NONE',  ( 2.500000000000000000, 0.000000000000000000, 0.000000000000000000 ) ) ;
#6937=ADVANCED_FACE ( 'NONE', ( #5205 ), #5912, .F. ) ;
#6976=FACE_OUTER_BOUND ( 'NONE', #13252, .T. ) ;
#6988=DIRECTION ( 'NONE',  ( -1.000000000000000000, -0.000000000000000000, -0.000000000000000000 ) ) ;
#6999=CARTESIAN_POINT ( 'NONE',  ( 2.500000000000000000, 2.357898499370433054, -1.951563910473907981E-15 ) ) ;
#7004=DIRECTION ( 'NONE',  ( -0.000000000000000000, 1.000000000000000000, 1.224646799147353207E-16 ) ) ;
#7032=CARTESIAN_POINT ( 'NONE',  ( 5.000000000000004441, 5.204748896376250699E-16, -4.250000000000000000 ) ) ;
#7044=EDGE_CURVE ( 'NONE', #8839, #7200, #5647, .T. ) ;
#7086=CARTESIAN_POINT ( 'NONE',  ( 2.500000000000000000, 1.178949249685213863, -2.042000000000001148 ) ) ;
#7097=SURFACE_STYLE_FILL_AREA ( #15898 ) ;
#7098=ORIENTED_EDGE ( 'NONE', *, *, #14944, .F. ) ;
#7113=EDGE_CURVE ( 'NONE', #7197, #12835, #9013, .T. ) ;
#7118=LINE ( 'NONE', #13391, #13640 ) ;
#7136=EDGE_CURVE ( 'NONE', #1523, #13974, #15788, .T. ) ;
#7140=VECTOR ( 'NONE', #9037, 1000.000000000000114 ) ;
#7151=EDGE_LOOP ( 'NONE', ( #9247, #13441 ) ) ;
#7152=CARTESIAN_POINT ( 'NONE',  ( 0.000000000000000000, 1.178949249685213863, -2.042000000000001148 ) ) ;
#7170=DIRECTION ( 'NONE',  ( 0.000000000000000000, 0.4999999999999993339, -0.8660254037844390407 ) ) ;
#7179=( LENGTH_UNIT ( ) NAMED_UNIT ( * ) SI_UNIT ( .MILLI., .METRE. ) );
#7191=CARTESIAN_POINT ( 'NONE',  ( 2.500000000000000000, 2.357898499370433054, -1.951563910473907981E-15 ) ) ;
#7197=VERTEX_POINT ( 'NONE', #10923 ) ;
#7200=VERTEX_POINT ( 'NONE', #28 ) ;
#7213=AXIS2_PLACEMENT_3D ( 'NONE', #4958, #8689, #1319 ) ;
#7215=PLANE ( 'NONE',  #3845 ) ;
#7263=LINE ( 'NONE', #1182, #1244 ) ;
#7270=LINE ( 'NONE', #12171, #6075 ) ;
#7281=DIRECTION ( 'NONE',  ( 0.000000000000000000, 1.000000000000000000, -1.471414886128461471E-15 ) ) ;
#7288=CARTESIAN_POINT ( 'NONE',  ( 0.2500000000000002220, 0.000000000000000000, 0.000000000000000000 ) ) ;
#7294=EDGE_CURVE ( 'NONE', #4992, #1523, #7263, .T. ) ;
#7305=DIRECTION ( 'NONE',  ( 0.000000000000000000, 0.000000000000000000, 1.000000000000000000 ) ) ;
#7365=FACE_OUTER_BOUND ( 'NONE', #10918, .T. ) ;
#7375=ADVANCED_FACE ( 'NONE', ( #15675 ), #4589, .F. ) ;
#7380=CARTESIAN_POINT ( 'NONE',  ( 2.500000000000000000, -2.629050547790028551E-15, -2.041999999999999815 ) ) ;
#7386=VERTEX_POINT ( 'NONE', #1265 ) ;
#7426=DIRECTION ( 'NONE',  ( 0.000000000000000000, -0.5000000000000012212, -0.8660254037844380415 ) ) ;
#7443=AXIS2_PLACEMENT_3D ( 'NONE', #6699, #13047, #9282 ) ;
#7444=DIRECTION ( 'NONE',  ( 0.000000000000000000, -0.4999999999999993894, 0.8660254037844389297 ) ) ;
#7460=ORIENTED_EDGE ( 'NONE', *, *, #4218, .T. ) ;
#7491=FACE_OUTER_BOUND ( 'NONE', #15303, .T. ) ;
#7492=ORIENTED_EDGE ( 'NONE', *, *, #673, .F. ) ;
#7552=VERTEX_POINT ( 'NONE', #12329 ) ;
#7559=FILL_AREA_STYLE ('',( #11105 ) ) ;
#7620=( GEOMETRIC_REPRESENTATION_CONTEXT ( 3 ) GLOBAL_UNCERTAINTY_ASSIGNED_CONTEXT ( ( #6265 ) ) GLOBAL_UNIT_ASSIGNED_CONTEXT ( ( #7179, #11848, #15749 ) ) REPRESENTATION_CONTEXT ( 'NONE', 'WORKASPACE' ) );
#7686=EDGE_CURVE ( 'NONE', #8590, #10453, #3829, .T. ) ;
#7700=EDGE_LOOP ( 'NONE', ( #9183, #12344, #13282, #8830 ) ) ;
#7702=VECTOR ( 'NONE', #5748, 1000.000000000000000 ) ;
#7730=SURFACE_SIDE_STYLE ('',( #12539 ) ) ;
#7733=DIRECTION ( 'NONE',  ( 1.000000000000000000, 0.000000000000000000, 0.000000000000000000 ) ) ;
#7752=ADVANCED_BREP_SHAPE_REPRESENTATION ( '', ( #14042, #3223 ), #15084 ) ;
#7787=VERTEX_POINT ( 'NONE', #14355 ) ;
#7842=EDGE_LOOP ( 'NONE', ( #1714, #4918 ) ) ;
#7860=DIRECTION ( 'NONE',  ( -1.000000000000000000, 0.000000000000000000, -0.000000000000000000 ) ) ;
#7979=ORIENTED_EDGE ( 'NONE', *, *, #14351, .F. ) ;
#8041=EDGE_LOOP ( 'NONE', ( #9436, #10937, #4079, #8572, #9497 ) ) ;
#8055=LINE ( 'NONE', #11738, #5328 ) ;
#8069=DIRECTION ( 'NONE',  ( 1.000000000000000000, 0.000000000000000000, 0.000000000000000000 ) ) ;
#8123=EDGE_CURVE ( 'NONE', #4992, #10194, #10682, .T. ) ;
#8133=MECHANICAL_DESIGN_GEOMETRIC_PRESENTATION_REPRESENTATION('',(#2178),#7620);
#8157=AXIS2_PLACEMENT_3D ( 'NONE', #9306, #14229, #10518 ) ;
#8162=APPLICATION_CONTEXT ( 'automotive_design' ) ;
#8170=CARTESIAN_POINT ( 'NONE',  ( 2.500000000000000000, 1.178949249685218525, 2.041999999999999371 ) ) ;
#8180=ADVANCED_FACE ( 'NONE', ( #6976 ), #14315, .F. ) ;
#8191=DIRECTION ( 'NONE',  ( 0.000000000000000000, 0.000000000000000000, -1.000000000000000000 ) ) ;
#8209=CIRCLE ( 'NONE', #2488, 2.500000000000000888 ) ;
#8226=AXIS2_PLACEMENT_3D ( 'NONE', #5553, #10487, #5475 ) ;
#8240=ADVANCED_FACE ( 'NONE', ( #3637 ), #2341, .T. ) ;
#8242=ORIENTED_EDGE ( 'NONE', *, *, #6490, .T. ) ;
#8245=( NAMED_UNIT ( * ) SI_UNIT ( $, .STERADIAN. ) SOLID_ANGLE_UNIT ( ) );
#8254=CARTESIAN_POINT ( 'NONE',  ( 0.000000000000000000, 2.357898499370433054, -1.951563910473907981E-15 ) ) ;
#8284=ORIENTED_EDGE ( 'NONE', *, *, #5320, .F. ) ;
#8290=ADVANCED_FACE ( 'NONE', ( #1127 ), #7215, .F. ) ;
#8299=DIRECTION ( 'NONE',  ( 0.000000000000000000, 0.000000000000000000, 1.000000000000000000 ) ) ;
#8325=AXIS2_PLACEMENT_3D ( 'NONE', #11795, #10837, #902 ) ;
#8351=EDGE_LOOP ( 'NONE', ( #5992, #8732, #3564, #14573 ) ) ;
#8380=CARTESIAN_POINT ( 'NONE',  ( -31.74999999999995737, 0.000000000000000000, 0.000000000000000000 ) ) ;
#8410=AXIS2_PLACEMENT_3D ( 'NONE', #2351, #3244, #4456 ) ;
#8411=CARTESIAN_POINT ( 'NONE',  ( 2.500000000000000000, 3.004629197474318851E-15, 2.042000000000000259 ) ) ;
#8426=TOROIDAL_SURFACE ( 'NONE', #8934, 2.700000000000001066, 0.2000000000000000111 ) ;
#8434=AXIS2_PLACEMENT_3D ( 'NONE', #15344, #3132, #636 ) ;
#8441=VECTOR ( 'NONE', #5533, 1000.000000000000000 ) ;
#8504=LINE ( 'NONE', #3632, #3825 ) ;
#8520=FACE_OUTER_BOUND ( 'NONE', #10647, .T. ) ;
#8521=CARTESIAN_POINT ( 'NONE',  ( 0.000000000000000000, 0.000000000000000000, 0.000000000000000000 ) ) ;
#8529=CARTESIAN_POINT ( 'NONE',  ( 2.500000000000000000, 0.000000000000000000, 0.000000000000000000 ) ) ;
#8534=ORIENTED_EDGE ( 'NONE', *, *, #11068, .T. ) ;
#8572=ORIENTED_EDGE ( 'NONE', *, *, #15904, .T. ) ;
#8590=VERTEX_POINT ( 'NONE', #7032 ) ;
#8614=DIRECTION ( 'NONE',  ( 0.000000000000000000, 1.000000000000000000, -1.471414886128461471E-15 ) ) ;
#8660=CARTESIAN_POINT ( 'NONE',  ( 2.500000000000000000, 0.000000000000000000, 0.000000000000000000 ) ) ;
#8689=DIRECTION ( 'NONE',  ( -1.000000000000000000, -0.000000000000000000, -0.000000000000000000 ) ) ;
#8691=UNCERTAINTY_MEASURE_WITH_UNIT (LENGTH_MEASURE( 1.000000000000000082E-05 ), #11921, 'distance_accuracy_value', 'NONE');
#8700=VERTEX_POINT ( 'NONE', #8170 ) ;
#8710=LINE ( 'NONE', #61, #7140 ) ;
#8732=ORIENTED_EDGE ( 'NONE', *, *, #7686, .T. ) ;
#8741=CARTESIAN_POINT ( 'NONE',  ( 2.500000000000000000, -1.178949249685213863, 2.042000000000002924 ) ) ;
#8830=ORIENTED_EDGE ( 'NONE', *, *, #8998, .F. ) ;
#8839=VERTEX_POINT ( 'NONE', #242 ) ;
#8852=PRODUCT_DEFINITION_CONTEXT ( 'detailed design', #327, 'design' ) ;
#8861=DIRECTION ( 'NONE',  ( 0.000000000000000000, 0.000000000000000000, 1.000000000000000000 ) ) ;
#8883=VERTEX_POINT ( 'NONE', #12727 ) ;
#8913=PLANE ( 'NONE',  #1202 ) ;
#8932=CARTESIAN_POINT ( 'NONE',  ( 5.200000000000002842, 0.000000000000000000, 0.000000000000000000 ) ) ;
#8933=DIRECTION ( 'NONE',  ( 0.000000000000000000, 0.000000000000000000, -1.000000000000000000 ) ) ;
#8934=AXIS2_PLACEMENT_3D ( 'NONE', #6644, #12514, #12600 ) ;
#8953=ADVANCED_FACE ( 'NONE', ( #15261 ), #8995, .F. ) ;
#8966=EDGE_LOOP ( 'NONE', ( #10172, #3956, #2108, #11233, #12060, #4481 ) ) ;
#8978=ADVANCED_FACE ( 'NONE', ( #5709 ), #2508, .T. ) ;
#8995=CONICAL_SURFACE ( 'NONE', #15182, 2.041999999999999815, 1.047197551196591858 ) ;
#8998=EDGE_CURVE ( 'NONE', #15784, #15426, #3306, .T. ) ;
#9013=CIRCLE ( 'NONE', #15726, 4.000000000000000000 ) ;
#9037=DIRECTION ( 'NONE',  ( -0.5000000000000051070, 1.060575238724903217E-16, -0.8660254037844355990 ) ) ;
#9088=DIRECTION ( 'NONE',  ( 0.000000000000000000, 0.000000000000000000, 1.000000000000000000 ) ) ;
#9099=ORIENTED_EDGE ( 'NONE', *, *, #3146, .F. ) ;
#9116=DIRECTION ( 'NONE',  ( 0.000000000000000000, 0.000000000000000000, 1.000000000000000000 ) ) ;
#9128=ORIENTED_EDGE ( 'NONE', *, *, #4009, .T. ) ;
#9183=ORIENTED_EDGE ( 'NONE', *, *, #5753, .F. ) ;
#9210=VERTEX_POINT ( 'NONE', #6436 ) ;
#9243=DIRECTION ( 'NONE',  ( 1.000000000000000000, 0.000000000000000000, 0.000000000000000000 ) ) ;
#9247=ORIENTED_EDGE ( 'NONE', *, *, #13260, .F. ) ;
#9252=CONICAL_SURFACE ( 'NONE', #12070, 2.041999999999999815, 1.047197551196591858 ) ;
#9263=PLANE ( 'NONE',  #6400 ) ;
#9282=DIRECTION ( 'NONE',  ( 0.000000000000000000, 0.000000000000000000, 1.000000000000000000 ) ) ;
#9306=CARTESIAN_POINT ( 'NONE',  ( 0.2500000000000002220, 0.000000000000000000, 4.000000000000000000 ) ) ;
#9322=ORIENTED_EDGE ( 'NONE', *, *, #7113, .F. ) ;
#9334=DIRECTION ( 'NONE',  ( -1.000000000000000000, -0.000000000000000000, -0.000000000000000000 ) ) ;
#9395=DIRECTION ( 'NONE',  ( -1.000000000000000000, -0.000000000000000000, -0.000000000000000000 ) ) ;
#9423=LINE ( 'NONE', #10399, #11021 ) ;
#9436=ORIENTED_EDGE ( 'NONE', *, *, #3313, .F. ) ;
#9497=ORIENTED_EDGE ( 'NONE', *, *, #4144, .T. ) ;
#9522=AXIS2_PLACEMENT_3D ( 'NONE', #15390, #6988, #1879 ) ;
#9552=EDGE_LOOP ( 'NONE', ( #1871, #622, #9764 ) ) ;
#9577=LINE ( 'NONE', #15890, #497 ) ;
#9605=CARTESIAN_POINT ( 'NONE',  ( 0.000000000000000000, 2.357898499370433054, -1.951563910473907981E-15 ) ) ;
#9613=DIRECTION ( 'NONE',  ( 0.000000000000000000, 0.000000000000000000, -1.000000000000000000 ) ) ;
#9619=EDGE_LOOP ( 'NONE', ( #14739, #1829 ) ) ;
#9637=FACE_OUTER_BOUND ( 'NONE', #15962, .T. ) ;
#9709=CIRCLE ( 'NONE', #2744, 2.041999999999999815 ) ;
#9717=ORIENTED_EDGE ( 'NONE', *, *, #3962, .T. ) ;
#9743=ADVANCED_FACE ( 'NONE', ( #13165 ), #3544, .F. ) ;
#9750=CARTESIAN_POINT ( 'NONE',  ( 2.500000000000000000, 2.357898499370433054, -1.951563910473907981E-15 ) ) ;
#9764=ORIENTED_EDGE ( 'NONE', *, *, #4218, .F. ) ;
#9784=CARTESIAN_POINT ( 'NONE',  ( 2.500000000000000000, 1.178949249685213863, -2.042000000000001148 ) ) ;
#9825=ORIENTED_EDGE ( 'NONE', *, *, #3975, .F. ) ;
#9881=CARTESIAN_POINT ( 'NONE',  ( 2.500000000000000000, -1.178949249685213863, 2.042000000000002924 ) ) ;
#9892=PLANE ( 'NONE',  #4870 ) ;
#9949=AXIS2_PLACEMENT_3D ( 'NONE', #4845, #1197, #4681 ) ;
#9961=EDGE_CURVE ( 'NONE', #15162, #5750, #12603, .T. ) ;
#9962=ORIENTED_EDGE ( 'NONE', *, *, #12479, .F. ) ;
#9964=DIRECTION ( 'NONE',  ( -1.000000000000000000, -0.000000000000000000, -0.000000000000000000 ) ) ;
#9996=CARTESIAN_POINT ( 'NONE',  ( 2.500000000000000000, -2.357898499370432610, 3.252606517456513302E-15 ) ) ;
#10008=VERTEX_POINT ( 'NONE', #1917 ) ;
#10031=VECTOR ( 'NONE', #13185, 1000.000000000000000 ) ;
#10052=LINE ( 'NONE', #14983, #235 ) ;
#10055=DIRECTION ( 'NONE',  ( 0.000000000000000000, -0.4999999999999992784, 0.8660254037844389297 ) ) ;
#10110=DIRECTION ( 'NONE',  ( 1.000000000000000000, 0.000000000000000000, 0.000000000000000000 ) ) ;
#10172=ORIENTED_EDGE ( 'NONE', *, *, #7136, .T. ) ;
#10194=VERTEX_POINT ( 'NONE', #5501 ) ;
#10199=EDGE_CURVE ( 'NONE', #7787, #15426, #7118, .T. ) ;
#10266=EDGE_LOOP ( 'NONE', ( #1348, #3272, #2987 ) ) ;
#10279=DIRECTION ( 'NONE',  ( 0.000000000000000000, 0.000000000000000000, -1.000000000000000000 ) ) ;
#10322=VERTEX_POINT ( 'NONE', #15326 ) ;
#10357=DIRECTION ( 'NONE',  ( 0.000000000000000000, -1.000000000000000000, 0.000000000000000000 ) ) ;
#10358=ORIENTED_EDGE ( 'NONE', *, *, #2998, .T. ) ;
#10380=ADVANCED_FACE ( 'NONE', ( #11664 ), #459, .T. ) ;
#10398=CARTESIAN_POINT ( 'NONE',  ( 25.00000000000000000, 2.789133085058098087E-16, -2.055000000000000160 ) ) ;
#10399=CARTESIAN_POINT ( 'NONE',  ( 2.500000000000000000, 1.178949249685218525, 2.041999999999999371 ) ) ;
#10409=ORIENTED_EDGE ( 'NONE', *, *, #13696, .F. ) ;
#10453=VERTEX_POINT ( 'NONE', #11974 ) ;
#10477=CIRCLE ( 'NONE', #8157, 0.2500000000000002220 ) ;
#10487=DIRECTION ( 'NONE',  ( -1.000000000000000000, -0.000000000000000000, -0.000000000000000000 ) ) ;
#10488=ADVANCED_FACE ( 'NONE', ( #9637 ), #1890, .F. ) ;
#10490=EDGE_CURVE ( 'NONE', #3781, #8839, #269, .T. ) ;
#10494=TOROIDAL_SURFACE ( 'NONE', #8434, 4.000000000000000000, 0.2500000000000000000 ) ;
#10508=CIRCLE ( 'NONE', #12288, 2.041999999999999815 ) ;
#10518=DIRECTION ( 'NONE',  ( 0.000000000000000000, 0.000000000000000000, -1.000000000000000000 ) ) ;
#10558=DIRECTION ( 'NONE',  ( -1.000000000000000000, -0.000000000000000000, -0.000000000000000000 ) ) ;
#10647=EDGE_LOOP ( 'NONE', ( #13730, #15484, #9099, #7492, #6569 ) ) ;
#10670=EDGE_CURVE ( 'NONE', #7200, #4793, #13495, .T. ) ;
#10682=LINE ( 'NONE', #13005, #10816 ) ;
#10748=VERTEX_POINT ( 'NONE', #2679 ) ;
#10773=PLANE ( 'NONE',  #6583 ) ;
#10816=VECTOR ( 'NONE', #668, 999.9999999999998863 ) ;
#10828=ADVANCED_FACE ( 'NONE', ( #2765 ), #4139, .T. ) ;
#10837=DIRECTION ( 'NONE',  ( -1.000000000000000000, -0.000000000000000000, -0.000000000000000000 ) ) ;
#10880=EDGE_LOOP ( 'NONE', ( #8284, #13666, #12856, #11212 ) ) ;
#10886=VECTOR ( 'NONE', #4047, 1000.000000000000000 ) ;
#10918=EDGE_LOOP ( 'NONE', ( #13031, #14644, #506, #1077, #4717 ) ) ;
#10923=CARTESIAN_POINT ( 'NONE',  ( 0.000000000000000000, 5.051668046482832750E-16, -4.000000000000000000 ) ) ;
#10924=EDGE_CURVE ( 'NONE', #8883, #13974, #2110, .T. ) ;
#10937=ORIENTED_EDGE ( 'NONE', *, *, #2152, .F. ) ;
#10947=COLOUR_RGB ( '', 0.31764706, 0.68627451, 0.89019608) ;
#10978=ORIENTED_EDGE ( 'NONE', *, *, #11590, .T. ) ;
#10980=COLOUR_RGB ( '', 0.31764706, 0.68627451, 0.89019608) ;
#10995=DIRECTION ( 'NONE',  ( 1.000000000000000000, 0.000000000000000000, 0.000000000000000000 ) ) ;
#11001=AXIS2_PLACEMENT_3D ( 'NONE', #1410, #15895, #8861 ) ;
#11021=VECTOR ( 'NONE', #467, 1000.000000000000000 ) ;
#11068=EDGE_CURVE ( 'NONE', #11174, #15077, #4865, .T. ) ;
#11075=DIRECTION ( 'NONE',  ( 0.000000000000000000, -1.000000000000000000, 1.471414886128461471E-15 ) ) ;
#11076=CARTESIAN_POINT ( 'NONE',  ( 2.500000000000000000, 1.178949249685213863, -2.042000000000001148 ) ) ;
#11105=FILL_AREA_STYLE_COLOUR ( '', #10980 ) ;
#11110=CARTESIAN_POINT ( 'NONE',  ( 25.00000000000000000, 2.055000000000000160, 0.000000000000000000 ) ) ;
#11160=ADVANCED_FACE ( 'NONE', ( #13903 ), #8426, .F. ) ;
#11173=VECTOR ( 'NONE', #13472, 1000.000000000000000 ) ;
#11174=VERTEX_POINT ( 'NONE', #15120 ) ;
#11212=ORIENTED_EDGE ( 'NONE', *, *, #14900, .F. ) ;
#11232=DIRECTION ( 'NONE',  ( 0.000000000000000000, -0.8660254037844390407, -0.4999999999999994449 ) ) ;
#11233=ORIENTED_EDGE ( 'NONE', *, *, #3313, .T. ) ;
#11275=ORIENTED_EDGE ( 'NONE', *, *, #13283, .F. ) ;
#11303=VECTOR ( 'NONE', #843, 1000.000000000000000 ) ;
#11324=EDGE_LOOP ( 'NONE', ( #13747, #6587, #7979 ) ) ;
#11343=( NAMED_UNIT ( * ) PLANE_ANGLE_UNIT ( ) SI_UNIT ( $, .RADIAN. ) );
#11375=ORIENTED_EDGE ( 'NONE', *, *, #14900, .T. ) ;
#11450=EDGE_LOOP ( 'NONE', ( #13368, #15475, #9962 ) ) ;
#11474=VERTEX_POINT ( 'NONE', #15923 ) ;
#11529=ADVANCED_FACE ( 'NONE', ( #5 ), #3460, .T. ) ;
#11590=EDGE_CURVE ( 'NONE', #1523, #15294, #13307, .T. ) ;
#11592=EDGE_LOOP ( 'NONE', ( #672, #3414, #3604, #12811 ) ) ;
#11609=ORIENTED_EDGE ( 'NONE', *, *, #5753, .T. ) ;
#11610=ORIENTED_EDGE ( 'NONE', *, *, #10670, .T. ) ;
#11634=FACE_OUTER_BOUND ( 'NONE', #7842, .T. ) ;
#11658=CYLINDRICAL_SURFACE ( 'NONE', #5031, 4.250000000000000000 ) ;
#11661=CARTESIAN_POINT ( 'NONE',  ( 2.500000000000000000, -1.178949249685218303, -2.041999999999998039 ) ) ;
#11664=FACE_OUTER_BOUND ( 'NONE', #8351, .T. ) ;
#11674=CARTESIAN_POINT ( 'NONE',  ( 5.000000000000004441, 0.000000000000000000, 0.000000000000000000 ) ) ;
#11704=AXIS2_PLACEMENT_3D ( 'NONE', #3837, #127, #5373 ) ;
#11736=DIRECTION ( 'NONE',  ( 1.000000000000000000, 0.000000000000000000, 0.000000000000000000 ) ) ;
#11737=DIRECTION ( 'NONE',  ( 1.000000000000000000, 0.000000000000000000, 0.000000000000000000 ) ) ;
#11738=CARTESIAN_POINT ( 'NONE',  ( 2.500000000000000000, -2.357898499370432610, 3.252606517456513302E-15 ) ) ;
#11755=LINE ( 'NONE', #3045, #14021 ) ;
#11761=UNCERTAINTY_MEASURE_WITH_UNIT (LENGTH_MEASURE( 1.000000000000000082E-05 ), #13754, 'distance_accuracy_value', 'NONE');
#11770=AXIS2_PLACEMENT_3D ( 'NONE', #13030, #11737, #844 ) ;
#11786=ORIENTED_EDGE ( 'NONE', *, *, #4164, .F. ) ;
#11795=CARTESIAN_POINT ( 'NONE',  ( 25.00000000000000000, 0.000000000000000000, 0.000000000000000000 ) ) ;
#11848=( NAMED_UNIT ( * ) PLANE_ANGLE_UNIT ( ) SI_UNIT ( $, .RADIAN. ) );
#11865=DIRECTION ( 'NONE',  ( -1.000000000000000000, -0.000000000000000000, -0.000000000000000000 ) ) ;
#11895=LINE ( 'NONE', #15560, #11303 ) ;
#11897=CARTESIAN_POINT ( 'NONE',  ( 0.000000000000000000, 0.000000000000000000, 0.000000000000000000 ) ) ;
#11921=( LENGTH_UNIT ( ) NAMED_UNIT ( * ) SI_UNIT ( .MILLI., .METRE. ) );
#11926=CARTESIAN_POINT ( 'NONE',  ( 5.000000000000000888, 0.000000000000000000, 0.000000000000000000 ) ) ;
#11961=ORIENTED_EDGE ( 'NONE', *, *, #2813, .F. ) ;
#11972=DIRECTION ( 'NONE',  ( 0.000000000000000000, 0.000000000000000000, 1.000000000000000000 ) ) ;
#11974=CARTESIAN_POINT ( 'NONE',  ( 5.000000000000004441, 0.000000000000000000, 4.250000000000000000 ) ) ;
#12034=DIRECTION ( 'NONE',  ( 0.000000000000000000, 0.5000000000000011102, 0.8660254037844380415 ) ) ;
#12053=EDGE_LOOP ( 'NONE', ( #10409, #9825, #11375, #9322 ) ) ;
#12060=ORIENTED_EDGE ( 'NONE', *, *, #6241, .F. ) ;
#12070=AXIS2_PLACEMENT_3D ( 'NONE', #8529, #2287, #7305 ) ;
#12090=AXIS2_PLACEMENT_3D ( 'NONE', #12340, #620, #2562 ) ;
#12091=DIRECTION ( 'NONE',  ( 1.000000000000000000, 0.000000000000000000, 0.000000000000000000 ) ) ;
#12116=CARTESIAN_POINT ( 'NONE',  ( 2.500000000000000000, 2.357898499370433054, -1.951563910473907981E-15 ) ) ;
#12127=DIRECTION ( 'NONE',  ( 0.000000000000000000, 0.000000000000000000, 1.000000000000000000 ) ) ;
#12142=EDGE_CURVE ( 'NONE', #11174, #3781, #8710, .T. ) ;
#12171=CARTESIAN_POINT ( 'NONE',  ( -31.74999999999995737, 3.061616997868384127E-16, -2.500000000000000888 ) ) ;
#12212=VERTEX_POINT ( 'NONE', #2545 ) ;
#12219=FACE_OUTER_BOUND ( 'NONE', #11592, .T. ) ;
#12237=TOROIDAL_SURFACE ( 'NONE', #5285, 4.000000000000000000, 0.2500000000000000000 ) ;
#12282=EDGE_CURVE ( 'NONE', #4793, #8839, #5060, .T. ) ;
#12288=AXIS2_PLACEMENT_3D ( 'NONE', #2498, #98, #2059 ) ;
#12322=DIRECTION ( 'NONE',  ( 0.000000000000000000, 0.000000000000000000, -1.000000000000000000 ) ) ;
#12329=CARTESIAN_POINT ( 'NONE',  ( 0.000000000000000000, -2.357898499370432610, 3.252606517456513302E-15 ) ) ;
#12340=CARTESIAN_POINT ( 'NONE',  ( -31.74999999999995737, 0.000000000000000000, 0.000000000000000000 ) ) ;
#12344=ORIENTED_EDGE ( 'NONE', *, *, #2301, .T. ) ;
#12363=ORIENTED_EDGE ( 'NONE', *, *, #9961, .T. ) ;
#12461=DIRECTION ( 'NONE',  ( 1.000000000000000000, 0.000000000000000000, 0.000000000000000000 ) ) ;
#12479=EDGE_CURVE ( 'NONE', #10194, #3781, #10508, .T. ) ;
#12508=STYLED_ITEM ( 'NONE', ( #3903 ), #14042 ) ;
#12514=DIRECTION ( 'NONE',  ( 1.000000000000000000, 0.000000000000000000, 0.000000000000000000 ) ) ;
#12531=DIRECTION ( 'NONE',  ( 0.000000000000000000, -0.5000000000000011102, -0.8660254037844379305 ) ) ;
#12539=SURFACE_STYLE_FILL_AREA ( #7559 ) ;
#12544=AXIS2_PLACEMENT_3D ( 'NONE', #12619, #9964, #9088 ) ;
#12557=VERTEX_POINT ( 'NONE', #5018 ) ;
#12600=DIRECTION ( 'NONE',  ( 0.000000000000000000, 0.000000000000000000, -1.000000000000000000 ) ) ;
#12603=CIRCLE ( 'NONE', #3335, 0.2000000000000000944 ) ;
#12619=CARTESIAN_POINT ( 'NONE',  ( 0.000000000000000000, 0.000000000000000000, 0.000000000000000000 ) ) ;
#12625=DIRECTION ( 'NONE',  ( 0.000000000000000000, 0.000000000000000000, -1.000000000000000000 ) ) ;
#12639=ADVANCED_FACE ( 'NONE', ( #27, #11634 ), #8913, .T. ) ;
#12726=CARTESIAN_POINT ( 'NONE',  ( -31.74999999999995737, 0.000000000000000000, 2.500000000000000888 ) ) ;
#12727=CARTESIAN_POINT ( 'NONE',  ( 0.000000000000000000, -1.178949249685213863, 2.042000000000002924 ) ) ;
#12766=CARTESIAN_POINT ( 'NONE',  ( -31.74999999999995737, 5.204748896376250699E-16, -4.250000000000000000 ) ) ;
#12811=ORIENTED_EDGE ( 'NONE', *, *, #2998, .F. ) ;
#12835=VERTEX_POINT ( 'NONE', #2175 ) ;
#12849=VECTOR ( 'NONE', #2894, 1000.000000000000000 ) ;
#12856=ORIENTED_EDGE ( 'NONE', *, *, #120, .F. ) ;
#12881=ORIENTED_EDGE ( 'NONE', *, *, #4944, .F. ) ;
#12940=CIRCLE ( 'NONE', #8325, 2.055000000000000160 ) ;
#12951=DIRECTION ( 'NONE',  ( 0.000000000000000000, 0.000000000000000000, 1.000000000000000000 ) ) ;
#12965=DIRECTION ( 'NONE',  ( 0.000000000000000000, 0.000000000000000000, 1.000000000000000000 ) ) ;
#13005=CARTESIAN_POINT ( 'NONE',  ( 2.500000000000000000, 2.357898499370433054, -1.951563910473907981E-15 ) ) ;
#13030=CARTESIAN_POINT ( 'NONE',  ( 5.000000000000000888, 4.250000000000000000, 0.000000000000000000 ) ) ;
#13031=ORIENTED_EDGE ( 'NONE', *, *, #7136, .F. ) ;
#13047=DIRECTION ( 'NONE',  ( -1.000000000000000000, -0.000000000000000000, -0.000000000000000000 ) ) ;
#13165=FACE_OUTER_BOUND ( 'NONE', #5537, .T. ) ;
#13174=CARTESIAN_POINT ( 'NONE',  ( 0.000000000000000000, -1.178949249685213863, 2.042000000000002924 ) ) ;
#13185=DIRECTION ( 'NONE',  ( 0.000000000000000000, -1.000000000000000000, 1.287488025362403787E-15 ) ) ;
#13193=CIRCLE ( 'NONE', #1333, 2.500000000000000888 ) ;
#13252=EDGE_LOOP ( 'NONE', ( #14591, #15307, #4520 ) ) ;
#13260=EDGE_CURVE ( 'NONE', #7787, #13811, #6876, .T. ) ;
#13265=EDGE_LOOP ( 'NONE', ( #13303, #4972 ) ) ;
#13282=ORIENTED_EDGE ( 'NONE', *, *, #10199, .T. ) ;
#13283=EDGE_CURVE ( 'NONE', #5750, #10008, #15125, .T. ) ;
#13303=ORIENTED_EDGE ( 'NONE', *, *, #3492, .T. ) ;
#13307=LINE ( 'NONE', #9605, #5321 ) ;
#13333=DIRECTION ( 'NONE',  ( 0.000000000000000000, 1.000000000000000000, -1.287488025362403787E-15 ) ) ;
#13368=ORIENTED_EDGE ( 'NONE', *, *, #2813, .T. ) ;
#13391=CARTESIAN_POINT ( 'NONE',  ( 25.00000000000000000, 0.000000000000000000, 2.055000000000000160 ) ) ;
#13400=ADVANCED_FACE ( 'NONE', ( #2229 ), #4978, .F. ) ;
#13404=LINE ( 'NONE', #9784, #11173 ) ;
#13424=ORIENTED_EDGE ( 'NONE', *, *, #641, .T. ) ;
#13438=ORIENTED_EDGE ( 'NONE', *, *, #10490, .T. ) ;
#13441=ORIENTED_EDGE ( 'NONE', *, *, #2301, .F. ) ;
#13466=LINE ( 'NONE', #11076, #12849 ) ;
#13472=DIRECTION ( 'NONE',  ( 0.000000000000000000, -1.000000000000000000, 1.287488025362403787E-15 ) ) ;
#13482=ORIENTED_EDGE ( 'NONE', *, *, #11068, .F. ) ;
#13495=LINE ( 'NONE', #9881, #4388 ) ;
#13512=AXIS2_PLACEMENT_3D ( 'NONE', #9750, #14688, #12322 ) ;
#13518=EDGE_LOOP ( 'NONE', ( #9717, #9128, #5075, #872 ) ) ;
#13593=CARTESIAN_POINT ( 'NONE',  ( 5.200000000000002842, 0.000000000000000000, 0.000000000000000000 ) ) ;
#13630=CARTESIAN_POINT ( 'NONE',  ( 2.500000000000000000, 1.178949249685213863, -2.042000000000001148 ) ) ;
#13639=AXIS2_PLACEMENT_3D ( 'NONE', #3243, #14166, #8191 ) ;
#13640=VECTOR ( 'NONE', #15840, 1000.000000000000000 ) ;
#13653=VECTOR ( 'NONE', #676, 1000.000000000000000 ) ;
#13656=DIRECTION ( 'NONE',  ( -0.5000000000000051070, 0.000000000000000000, 0.8660254037844355990 ) ) ;
#13666=ORIENTED_EDGE ( 'NONE', *, *, #13696, .T. ) ;
#13696=EDGE_CURVE ( 'NONE', #9210, #7197, #5280, .T. ) ;
#13715=ORIENTED_EDGE ( 'NONE', *, *, #8998, .T. ) ;
#13730=ORIENTED_EDGE ( 'NONE', *, *, #6241, .T. ) ;
#13738=SHAPE_DEFINITION_REPRESENTATION ( #4738, #790 ) ;
#13747=ORIENTED_EDGE ( 'NONE', *, *, #6490, .F. ) ;
#13754=( LENGTH_UNIT ( ) NAMED_UNIT ( * ) SI_UNIT ( .MILLI., .METRE. ) );
#13811=VERTEX_POINT ( 'NONE', #10398 ) ;
#13828=CARTESIAN_POINT ( 'NONE',  ( 5.000000000000004441, 0.000000000000000000, 0.000000000000000000 ) ) ;
#13854=FACE_OUTER_BOUND ( 'NONE', #10266, .T. ) ;
#13856=CARTESIAN_POINT ( 'NONE',  ( 24.55500000000002103, 3.061616997868384620E-16, -2.500000000000001332 ) ) ;
#13899=CARTESIAN_POINT ( 'NONE',  ( 5.200000000000002842, 0.000000000000000000, -2.700000000000001066 ) ) ;
#13903=FACE_OUTER_BOUND ( 'NONE', #424, .T. ) ;
#13974=VERTEX_POINT ( 'NONE', #2367 ) ;
#13980=DIRECTION ( 'NONE',  ( -0.000000000000000000, 0.000000000000000000, 1.000000000000000000 ) ) ;
#14021=VECTOR ( 'NONE', #15655, 1000.000000000000114 ) ;
#14042=MANIFOLD_SOLID_BREP ( 'Hex', #15917 ) ;
#14102=DIRECTION ( 'NONE',  ( -1.000000000000000000, -0.000000000000000000, -0.000000000000000000 ) ) ;
#14133=DIRECTION ( 'NONE',  ( -1.000000000000000000, -0.000000000000000000, -0.000000000000000000 ) ) ;
#14166=DIRECTION ( 'NONE',  ( 1.000000000000000000, 0.000000000000000000, 0.000000000000000000 ) ) ;
#14194=ORIENTED_EDGE ( 'NONE', *, *, #7044, .T. ) ;
#14219=DIRECTION ( 'NONE',  ( 0.000000000000000000, 1.000000000000000000, -1.224646799147353207E-16 ) ) ;
#14229=DIRECTION ( 'NONE',  ( 0.000000000000000000, -1.000000000000000000, 0.000000000000000000 ) ) ;
#14279=DIRECTION ( 'NONE',  ( -1.000000000000000000, -0.000000000000000000, -0.000000000000000000 ) ) ;
#14311=ADVANCED_FACE ( 'NONE', ( #8520 ), #10773, .F. ) ;
#14314=CARTESIAN_POINT ( 'NONE',  ( 5.200000000000002842, 0.000000000000000000, 0.000000000000000000 ) ) ;
#14315=PLANE ( 'NONE',  #13639 ) ;
#14351=EDGE_CURVE ( 'NONE', #7200, #15077, #3731, .T. ) ;
#14355=CARTESIAN_POINT ( 'NONE',  ( 25.00000000000000000, 0.000000000000000000, 2.055000000000000160 ) ) ;
#14388=EDGE_LOOP ( 'NONE', ( #5874, #4605, #5184 ) ) ;
#14438=CARTESIAN_POINT ( 'NONE',  ( 0.2500000000000002220, 0.000000000000000000, 0.000000000000000000 ) ) ;
#14444=AXIS2_PLACEMENT_3D ( 'NONE', #6999, #4408, #5620 ) ;
#14450=ORIENTED_EDGE ( 'NONE', *, *, #8123, .F. ) ;
#14495=DIRECTION ( 'NONE',  ( 0.000000000000000000, 0.4999999999999993339, -0.8660254037844390407 ) ) ;
#14504=CARTESIAN_POINT ( 'NONE',  ( 2.500000000000000000, 2.357898499370433054, -1.951563910473907981E-15 ) ) ;
#14518=SHAPE_REPRESENTATION_RELATIONSHIP ( 'NONE' , 'NONE' ,  #790, #7752 ) ;
#14541=DIRECTION ( 'NONE',  ( 0.000000000000000000, -0.5000000000000012212, -0.8660254037844380415 ) ) ;
#14573=ORIENTED_EDGE ( 'NONE', *, *, #3975, .T. ) ;
#14591=ORIENTED_EDGE ( 'NONE', *, *, #12282, .F. ) ;
#14623=ADVANCED_FACE ( 'NONE', ( #4475 ), #11658, .T. ) ;
#14644=ORIENTED_EDGE ( 'NONE', *, *, #7294, .F. ) ;
#14688=DIRECTION ( 'NONE',  ( 1.000000000000000000, 0.000000000000000000, 0.000000000000000000 ) ) ;
#14709=CARTESIAN_POINT ( 'NONE',  ( 2.500000000000000000, -1.178949249685213863, 2.042000000000002924 ) ) ;
#14716=ADVANCED_FACE ( 'NONE', ( #15483 ), #12237, .T. ) ;
#14739=ORIENTED_EDGE ( 'NONE', *, *, #3962, .F. ) ;
#14757=ORIENTED_EDGE ( 'NONE', *, *, #15028, .F. ) ;
#14774=ORIENTED_EDGE ( 'NONE', *, *, #3492, .F. ) ;
#14783=ADVANCED_FACE ( 'NONE', ( #4936 ), #3715, .F. ) ;
#14798=CARTESIAN_POINT ( 'NONE',  ( 2.500000000000000000, 0.000000000000000000, 2.041999999999999815 ) ) ;
#14824=LINE ( 'NONE', #15298, #10886 ) ;
#14829=DIRECTION ( 'NONE',  ( 1.000000000000000000, 0.000000000000000000, 0.000000000000000000 ) ) ;
#14879=CIRCLE ( 'NONE', #3271, 4.250000000000000000 ) ;
#14900=EDGE_CURVE ( 'NONE', #12212, #12835, #10477, .T. ) ;
#14927=ORIENTED_EDGE ( 'NONE', *, *, #4623, .F. ) ;
#14939=CARTESIAN_POINT ( 'NONE',  ( 2.500000000000000000, 2.357898499370433054, -1.951563910473907981E-15 ) ) ;
#14944=EDGE_CURVE ( 'NONE', #10748, #10008, #4276, .T. ) ;
#14956=AXIS2_PLACEMENT_3D ( 'NONE', #8741, #3797, #12034 ) ;
#14983=CARTESIAN_POINT ( 'NONE',  ( 2.500000000000000000, -1.178949249685213863, 2.042000000000002924 ) ) ;
#15028=EDGE_CURVE ( 'NONE', #15784, #10748, #7270, .T. ) ;
#15077=VERTEX_POINT ( 'NONE', #8411 ) ;
#15084=( GEOMETRIC_REPRESENTATION_CONTEXT ( 3 ) GLOBAL_UNCERTAINTY_ASSIGNED_CONTEXT ( ( #8691 ) ) GLOBAL_UNIT_ASSIGNED_CONTEXT ( ( #11921, #3294, #8245 ) ) REPRESENTATION_CONTEXT ( 'NONE', 'WORKASPACE' ) );
#15120=CARTESIAN_POINT ( 'NONE',  ( 3.678949249685231848, 0.000000000000000000, 0.000000000000000000 ) ) ;
#15125=CIRCLE ( 'NONE', #6834, 2.700000000000001066 ) ;
#15144=CIRCLE ( 'NONE', #939, 4.250000000000000000 ) ;
#15154=VECTOR ( 'NONE', #8614, 1000.000000000000000 ) ;
#15162=VERTEX_POINT ( 'NONE', #2640 ) ;
#15182=AXIS2_PLACEMENT_3D ( 'NONE', #1987, #14279, #4495 ) ;
#15230=VERTEX_POINT ( 'NONE', #13630 ) ;
#15261=FACE_OUTER_BOUND ( 'NONE', #4200, .T. ) ;
#15293=ADVANCED_FACE ( 'NONE', ( #4260 ), #10494, .T. ) ;
#15294=VERTEX_POINT ( 'NONE', #1909 ) ;
#15298=CARTESIAN_POINT ( 'NONE',  ( 2.500000000000000000, -2.357898499370432610, 3.252606517456513302E-15 ) ) ;
#15303=EDGE_LOOP ( 'NONE', ( #1504, #11609, #15454, #272 ) ) ;
#15304=CARTESIAN_POINT ( 'NONE',  ( 2.500000000000000000, -2.357898499370432610, 3.252606517456513302E-15 ) ) ;
#15307=ORIENTED_EDGE ( 'NONE', *, *, #10670, .F. ) ;
#15313=VECTOR ( 'NONE', #7426, 999.9999999999998863 ) ;
#15326=CARTESIAN_POINT ( 'NONE',  ( 2.500000000000000000, -1.178949249685213863, 2.042000000000002924 ) ) ;
#15344=CARTESIAN_POINT ( 'NONE',  ( 0.2500000000000002220, 0.000000000000000000, 0.000000000000000000 ) ) ;
#15390=CARTESIAN_POINT ( 'NONE',  ( 2.500000000000000000, 0.000000000000000000, 0.000000000000000000 ) ) ;
#15401=LINE ( 'NONE', #3025, #1198 ) ;
#15405=VECTOR ( 'NONE', #9395, 1000.000000000000000 ) ;
#15426=VERTEX_POINT ( 'NONE', #4180 ) ;
#15454=ORIENTED_EDGE ( 'NONE', *, *, #6802, .F. ) ;
#15460=PRODUCT ( 'socket head cap screw_iso_ISO 4762 M5 x 20 - 20N', 'socket head cap screw_iso_ISO 4762 M5 x 20 - 20N', '', ( #5267 ) ) ;
#15475=ORIENTED_EDGE ( 'NONE', *, *, #673, .T. ) ;
#15483=FACE_OUTER_BOUND ( 'NONE', #12053, .T. ) ;
#15484=ORIENTED_EDGE ( 'NONE', *, *, #4144, .F. ) ;
#15560=CARTESIAN_POINT ( 'NONE',  ( -31.74999999999995737, 0.000000000000000000, 4.250000000000000000 ) ) ;
#15575=ADVANCED_FACE ( 'NONE', ( #7491 ), #2456, .T. ) ;
#15627=MECHANICAL_DESIGN_GEOMETRIC_PRESENTATION_REPRESENTATION('',(#12508),#4268);
#15655=DIRECTION ( 'NONE',  ( 0.000000000000000000, -0.5000000000000011102, -0.8660254037844379305 ) ) ;
#15675=FACE_OUTER_BOUND ( 'NONE', #14388, .T. ) ;
#15726=AXIS2_PLACEMENT_3D ( 'NONE', #8521, #1220, #12127 ) ;
#15741=DIRECTION ( 'NONE',  ( 0.000000000000000000, 0.000000000000000000, -1.000000000000000000 ) ) ;
#15749=( NAMED_UNIT ( * ) SI_UNIT ( $, .STERADIAN. ) SOLID_ANGLE_UNIT ( ) );
#15784=VERTEX_POINT ( 'NONE', #13856 ) ;
#15788=LINE ( 'NONE', #4703, #2028 ) ;
#15808=DIRECTION ( 'NONE',  ( 0.000000000000000000, 0.000000000000000000, 1.000000000000000000 ) ) ;
#15840=DIRECTION ( 'NONE',  ( -0.7071067811865306973, 0.000000000000000000, 0.7071067811865643371 ) ) ;
#15854=LINE ( 'NONE', #3555, #7702 ) ;
#15885=CARTESIAN_POINT ( 'NONE',  ( 2.500000000000000000, -2.357898499370432610, 3.252606517456513302E-15 ) ) ;
#15890=CARTESIAN_POINT ( 'NONE',  ( 0.000000000000000000, -2.357898499370432610, 3.252606517456513302E-15 ) ) ;
#15895=DIRECTION ( 'NONE',  ( -1.000000000000000000, -0.000000000000000000, -0.000000000000000000 ) ) ;
#15898=FILL_AREA_STYLE ('',( #6034 ) ) ;
#15899=AXIS2_PLACEMENT_3D ( 'NONE', #266, #10110, #2493 ) ;
#15900=ORIENTED_EDGE ( 'NONE', *, *, #10924, .T. ) ;
#15904=EDGE_CURVE ( 'NONE', #8839, #7386, #8055, .T. ) ;
#15908=DIRECTION ( 'NONE',  ( -1.000000000000000000, -0.000000000000000000, -0.000000000000000000 ) ) ;
#15917=CLOSED_SHELL ( 'NONE', ( #8953, #15293, #11160, #14623, #2030, #15575, #12639, #3364, #8978, #11529, #4230, #10380, #6937, #14716, #5781, #9743, #8240, #10828, #14311, #10488, #7375, #8180, #13400, #8290, #6029, #14783, #6325 ) ) ;
#15923=CARTESIAN_POINT ( 'NONE',  ( 2.500000000000000000, 1.768423874527824902, 1.020999999999999019 ) ) ;
#15934=DIRECTION ( 'NONE',  ( 0.000000000000000000, 0.000000000000000000, -1.000000000000000000 ) ) ;
#15962=EDGE_LOOP ( 'NONE', ( #10978, #1473, #11961, #14450, #3658 ) ) ;
ENDSEC;
END-ISO-10303-21;
